ISO-10303-21;
HEADER;
/* Generated by software containing ST-Developer
 * from STEP Tools, Inc. (www.steptools.com) 
 */

FILE_DESCRIPTION(
/* description */ ('Telescoping shaft support with lock collar'),
/* implementation_level */ '2;1');

FILE_NAME(
/* name */ 'Socket Set Screw - M5x8.step',
/* time_stamp */ '2026-10-27T10:48:51-07:00',
/* author */ (''),
/* organization */ (''),
/* preprocessor_version */ 'ST-DEVELOPER v20.2',
/* originating_system */ 'Autodesk Translation Framework v15.17.0.0',
/* authorisation */ '');

FILE_SCHEMA (('AUTOMOTIVE_DESIGN { 1 0 10303 214 3 1 1 }'));
ENDSEC;

DATA;
#10=MECHANICAL_DESIGN_GEOMETRIC_PRESENTATION_REPRESENTATION('',(#259),#7349);
#175=CONICAL_SURFACE('',#4637,0.235,0.785398163397448);
#176=CONICAL_SURFACE('',#4641,0.2125,0.785398163397448);
#219=SHAPE_REPRESENTATION_RELATIONSHIP('SRR','None',#7463,#239);
#239=ADVANCED_BREP_SHAPE_REPRESENTATION('',(#278),#7347);
#259=STYLED_ITEM('',(#7634),#278);
#278=MANIFOLD_SOLID_BREP('Body1',#3983);
#357=FACE_BOUND('',#1004,.T.);
#475=PLANE('',#4628);
#476=PLANE('',#4629);
#477=PLANE('',#4630);
#478=PLANE('',#4631);
#479=PLANE('',#4632);
#480=PLANE('',#4633);
#481=PLANE('',#4634);
#482=PLANE('',#4635);
#483=PLANE('',#4643);
#692=FACE_OUTER_BOUND('',#996,.T.);
#693=FACE_OUTER_BOUND('',#997,.T.);
#694=FACE_OUTER_BOUND('',#998,.T.);
#695=FACE_OUTER_BOUND('',#999,.T.);
#696=FACE_OUTER_BOUND('',#1000,.T.);
#697=FACE_OUTER_BOUND('',#1001,.T.);
#698=FACE_OUTER_BOUND('',#1002,.T.);
#699=FACE_OUTER_BOUND('',#1003,.T.);
#700=FACE_OUTER_BOUND('',#1005,.T.);
#701=FACE_OUTER_BOUND('',#1006,.T.);
#702=FACE_OUTER_BOUND('',#1007,.T.);
#703=FACE_OUTER_BOUND('',#1008,.T.);
#996=EDGE_LOOP('',(#3546,#3547,#3548,#3549));
#997=EDGE_LOOP('',(#3550,#3551,#3552,#3553));
#998=EDGE_LOOP('',(#3554,#3555,#3556,#3557));
#999=EDGE_LOOP('',(#3558,#3559,#3560,#3561));
#1000=EDGE_LOOP('',(#3562,#3563,#3564,#3565));
#1001=EDGE_LOOP('',(#3566,#3567,#3568,#3569));
#1002=EDGE_LOOP('',(#3570,#3571,#3572,#3573,#3574,#3575));
#1003=EDGE_LOOP('',(#3576));
#1004=EDGE_LOOP('',(#3577,#3578,#3579,#3580,#3581,#3582));
#1005=EDGE_LOOP('',(#3583,#3584,#3585,#3586));
#1006=EDGE_LOOP('',(#3587,#3588,#3589,#3590));
#1007=EDGE_LOOP('',(#3591,#3592,#3593,#3594));
#1008=EDGE_LOOP('',(#3595));
#1262=LINE('',#7143,#1542);
#1263=LINE('',#7145,#1543);
#1264=LINE('',#7147,#1544);
#1265=LINE('',#7148,#1545);
#1266=LINE('',#7151,#1546);
#1267=LINE('',#7153,#1547);
#1268=LINE('',#7154,#1548);
#1269=LINE('',#7157,#1549);
#1270=LINE('',#7159,#1550);
#1271=LINE('',#7160,#1551);
#1272=LINE('',#7163,#1552);
#1273=LINE('',#7165,#1553);
#1274=LINE('',#7166,#1554);
#1275=LINE('',#7169,#1555);
#1276=LINE('',#7171,#1556);
#1277=LINE('',#7172,#1557);
#1278=LINE('',#7174,#1558);
#1279=LINE('',#7175,#1559);
#1280=LINE('',#7183,#1560);
#1281=LINE('',#7187,#1561);
#1282=LINE('',#7191,#1562);
#1542=VECTOR('',#5786,1.);
#1543=VECTOR('',#5787,1.);
#1544=VECTOR('',#5788,1.);
#1545=VECTOR('',#5789,1.);
#1546=VECTOR('',#5792,1.);
#1547=VECTOR('',#5793,1.);
#1548=VECTOR('',#5794,1.);
#1549=VECTOR('',#5797,1.);
#1550=VECTOR('',#5798,1.);
#1551=VECTOR('',#5799,1.);
#1552=VECTOR('',#5802,1.);
#1553=VECTOR('',#5803,1.);
#1554=VECTOR('',#5804,1.);
#1555=VECTOR('',#5807,1.);
#1556=VECTOR('',#5808,1.);
#1557=VECTOR('',#5809,1.);
#1558=VECTOR('',#5812,1.);
#1559=VECTOR('',#5813,1.);
#1560=VECTOR('',#5824,0.235);
#1561=VECTOR('',#5829,0.25);
#1562=VECTOR('',#5834,0.2125);
#1786=CIRCLE('',#4636,0.22);
#1787=CIRCLE('',#4638,0.24505);
#1788=CIRCLE('',#4640,0.24505);
#1789=CIRCLE('',#4642,0.175);
#2097=VERTEX_POINT('',#7141);
#2098=VERTEX_POINT('',#7142);
#2099=VERTEX_POINT('',#7144);
#2100=VERTEX_POINT('',#7146);
#2101=VERTEX_POINT('',#7150);
#2102=VERTEX_POINT('',#7152);
#2103=VERTEX_POINT('',#7156);
#2104=VERTEX_POINT('',#7158);
#2105=VERTEX_POINT('',#7162);
#2106=VERTEX_POINT('',#7164);
#2107=VERTEX_POINT('',#7168);
#2108=VERTEX_POINT('',#7170);
#2109=VERTEX_POINT('',#7178);
#2110=VERTEX_POINT('',#7181);
#2111=VERTEX_POINT('',#7185);
#2112=VERTEX_POINT('',#7189);
#2585=EDGE_CURVE('',#2097,#2098,#1262,.T.);
#2586=EDGE_CURVE('',#2097,#2099,#1263,.T.);
#2587=EDGE_CURVE('',#2099,#2100,#1264,.T.);
#2588=EDGE_CURVE('',#2098,#2100,#1265,.T.);
#2589=EDGE_CURVE('',#2101,#2097,#1266,.T.);
#2590=EDGE_CURVE('',#2101,#2102,#1267,.T.);
#2591=EDGE_CURVE('',#2102,#2099,#1268,.T.);
#2592=EDGE_CURVE('',#2103,#2101,#1269,.T.);
#2593=EDGE_CURVE('',#2103,#2104,#1270,.T.);
#2594=EDGE_CURVE('',#2104,#2102,#1271,.T.);
#2595=EDGE_CURVE('',#2105,#2103,#1272,.T.);
#2596=EDGE_CURVE('',#2105,#2106,#1273,.T.);
#2597=EDGE_CURVE('',#2106,#2104,#1274,.T.);
#2598=EDGE_CURVE('',#2107,#2105,#1275,.T.);
#2599=EDGE_CURVE('',#2107,#2108,#1276,.T.);
#2600=EDGE_CURVE('',#2108,#2106,#1277,.T.);
#2601=EDGE_CURVE('',#2098,#2107,#1278,.T.);
#2602=EDGE_CURVE('',#2100,#2108,#1279,.T.);
#2603=EDGE_CURVE('',#2109,#2109,#1786,.T.);
#2604=EDGE_CURVE('',#2110,#2110,#1787,.T.);
#2605=EDGE_CURVE('',#2110,#2109,#1280,.T.);
#2606=EDGE_CURVE('',#2111,#2111,#1788,.F.);
#2607=EDGE_CURVE('',#2111,#2110,#1281,.T.);
#2608=EDGE_CURVE('',#2112,#2112,#1789,.T.);
#2609=EDGE_CURVE('',#2112,#2111,#1282,.T.);
#3546=ORIENTED_EDGE('',*,*,#2585,.F.);
#3547=ORIENTED_EDGE('',*,*,#2586,.T.);
#3548=ORIENTED_EDGE('',*,*,#2587,.T.);
#3549=ORIENTED_EDGE('',*,*,#2588,.F.);
#3550=ORIENTED_EDGE('',*,*,#2589,.F.);
#3551=ORIENTED_EDGE('',*,*,#2590,.T.);
#3552=ORIENTED_EDGE('',*,*,#2591,.T.);
#3553=ORIENTED_EDGE('',*,*,#2586,.F.);
#3554=ORIENTED_EDGE('',*,*,#2592,.F.);
#3555=ORIENTED_EDGE('',*,*,#2593,.T.);
#3556=ORIENTED_EDGE('',*,*,#2594,.T.);
#3557=ORIENTED_EDGE('',*,*,#2590,.F.);
#3558=ORIENTED_EDGE('',*,*,#2595,.F.);
#3559=ORIENTED_EDGE('',*,*,#2596,.T.);
#3560=ORIENTED_EDGE('',*,*,#2597,.T.);
#3561=ORIENTED_EDGE('',*,*,#2593,.F.);
#3562=ORIENTED_EDGE('',*,*,#2598,.F.);
#3563=ORIENTED_EDGE('',*,*,#2599,.T.);
#3564=ORIENTED_EDGE('',*,*,#2600,.T.);
#3565=ORIENTED_EDGE('',*,*,#2596,.F.);
#3566=ORIENTED_EDGE('',*,*,#2601,.F.);
#3567=ORIENTED_EDGE('',*,*,#2588,.T.);
#3568=ORIENTED_EDGE('',*,*,#2602,.T.);
#3569=ORIENTED_EDGE('',*,*,#2599,.F.);
#3570=ORIENTED_EDGE('',*,*,#2602,.F.);
#3571=ORIENTED_EDGE('',*,*,#2587,.F.);
#3572=ORIENTED_EDGE('',*,*,#2591,.F.);
#3573=ORIENTED_EDGE('',*,*,#2594,.F.);
#3574=ORIENTED_EDGE('',*,*,#2597,.F.);
#3575=ORIENTED_EDGE('',*,*,#2600,.F.);
#3576=ORIENTED_EDGE('',*,*,#2603,.F.);
#3577=ORIENTED_EDGE('',*,*,#2585,.T.);
#3578=ORIENTED_EDGE('',*,*,#2601,.T.);
#3579=ORIENTED_EDGE('',*,*,#2598,.T.);
#3580=ORIENTED_EDGE('',*,*,#2595,.T.);
#3581=ORIENTED_EDGE('',*,*,#2592,.T.);
#3582=ORIENTED_EDGE('',*,*,#2589,.T.);
#3583=ORIENTED_EDGE('',*,*,#2604,.F.);
#3584=ORIENTED_EDGE('',*,*,#2605,.T.);
#3585=ORIENTED_EDGE('',*,*,#2603,.T.);
#3586=ORIENTED_EDGE('',*,*,#2605,.F.);
#3587=ORIENTED_EDGE('',*,*,#2606,.F.);
#3588=ORIENTED_EDGE('',*,*,#2607,.T.);
#3589=ORIENTED_EDGE('',*,*,#2604,.T.);
#3590=ORIENTED_EDGE('',*,*,#2607,.F.);
#3591=ORIENTED_EDGE('',*,*,#2608,.F.);
#3592=ORIENTED_EDGE('',*,*,#2609,.T.);
#3593=ORIENTED_EDGE('',*,*,#2606,.T.);
#3594=ORIENTED_EDGE('',*,*,#2609,.F.);
#3595=ORIENTED_EDGE('',*,*,#2608,.T.);
#3735=CYLINDRICAL_SURFACE('',#4639,0.24505);
#3935=ADVANCED_FACE('',(#692),#475,.F.);
#3936=ADVANCED_FACE('',(#693),#476,.F.);
#3937=ADVANCED_FACE('',(#694),#477,.F.);
#3938=ADVANCED_FACE('',(#695),#478,.F.);
#3939=ADVANCED_FACE('',(#696),#479,.F.);
#3940=ADVANCED_FACE('',(#697),#480,.F.);
#3941=ADVANCED_FACE('',(#698),#481,.F.);
#3942=ADVANCED_FACE('',(#699,#357),#482,.T.);
#3943=ADVANCED_FACE('',(#700),#175,.T.);
#3944=ADVANCED_FACE('',(#701),#3735,.T.);
#3945=ADVANCED_FACE('',(#702),#176,.T.);
#3946=ADVANCED_FACE('',(#703),#483,.T.);
#3983=CLOSED_SHELL('',(#3935,#3936,#3937,#3938,#3939,#3940,#3941,#3942,
#3943,#3944,#3945,#3946));
#4627=AXIS2_PLACEMENT_3D('',#7139,#5782,#5783);
#4628=AXIS2_PLACEMENT_3D('',#7140,#5784,#5785);
#4629=AXIS2_PLACEMENT_3D('',#7149,#5790,#5791);
#4630=AXIS2_PLACEMENT_3D('',#7155,#5795,#5796);
#4631=AXIS2_PLACEMENT_3D('',#7161,#5800,#5801);
#4632=AXIS2_PLACEMENT_3D('',#7167,#5805,#5806);
#4633=AXIS2_PLACEMENT_3D('',#7173,#5810,#5811);
#4634=AXIS2_PLACEMENT_3D('',#7176,#5814,#5815);
#4635=AXIS2_PLACEMENT_3D('',#7177,#5816,#5817);
#4636=AXIS2_PLACEMENT_3D('',#7179,#5818,#5819);
#4637=AXIS2_PLACEMENT_3D('',#7180,#5820,#5821);
#4638=AXIS2_PLACEMENT_3D('',#7182,#5822,#5823);
#4639=AXIS2_PLACEMENT_3D('',#7184,#5825,#5826);
#4640=AXIS2_PLACEMENT_3D('',#7186,#5827,#5828);
#4641=AXIS2_PLACEMENT_3D('',#7188,#5830,#5831);
#4642=AXIS2_PLACEMENT_3D('',#7190,#5832,#5833);
#4643=AXIS2_PLACEMENT_3D('',#7192,#5835,#5836);
#5782=DIRECTION('axis',(0.,0.,1.));
#5783=DIRECTION('refdir',(1.,0.,0.));
#5784=DIRECTION('center_axis',(0.866025403784439,0.,-0.5));
#5785=DIRECTION('ref_axis',(0.5,0.,0.866025403784439));
#5786=DIRECTION('',(0.5,0.,0.866025403784439));
#5787=DIRECTION('',(0.,-1.,0.));
#5788=DIRECTION('',(0.5,0.,0.866025403784439));
#5789=DIRECTION('',(0.,-1.,0.));
#5790=DIRECTION('center_axis',(1.92296268638356E-16,0.,-1.));
#5791=DIRECTION('ref_axis',(1.,0.,1.92296268638356E-16));
#5792=DIRECTION('',(1.,0.,1.92296268638356E-16));
#5793=DIRECTION('',(0.,-1.,0.));
#5794=DIRECTION('',(1.,0.,1.92296268638356E-16));
#5795=DIRECTION('center_axis',(-0.866025403784439,0.,-0.5));
#5796=DIRECTION('ref_axis',(0.5,0.,-0.866025403784439));
#5797=DIRECTION('',(0.5,0.,-0.866025403784439));
#5798=DIRECTION('',(0.,-1.,0.));
#5799=DIRECTION('',(0.5,0.,-0.866025403784438));
#5800=DIRECTION('center_axis',(-0.866025403784439,0.,0.5));
#5801=DIRECTION('ref_axis',(-0.5,0.,-0.866025403784439));
#5802=DIRECTION('',(-0.5,0.,-0.866025403784439));
#5803=DIRECTION('',(0.,-1.,0.));
#5804=DIRECTION('',(-0.5,0.,-0.866025403784439));
#5805=DIRECTION('center_axis',(-1.92296268638356E-16,0.,1.));
#5806=DIRECTION('ref_axis',(-1.,0.,-1.92296268638356E-16));
#5807=DIRECTION('',(-1.,0.,-1.92296268638356E-16));
#5808=DIRECTION('',(0.,-1.,0.));
#5809=DIRECTION('',(-1.,0.,-1.92296268638356E-16));
#5810=DIRECTION('center_axis',(0.866025403784439,0.,0.5));
#5811=DIRECTION('ref_axis',(-0.5,0.,0.866025403784439));
#5812=DIRECTION('',(-0.5,0.,0.866025403784439));
#5813=DIRECTION('',(-0.5,0.,0.866025403784439));
#5814=DIRECTION('center_axis',(0.,-1.,0.));
#5815=DIRECTION('ref_axis',(0.,0.,-1.));
#5816=DIRECTION('center_axis',(0.,1.,0.));
#5817=DIRECTION('ref_axis',(0.,0.,1.));
#5818=DIRECTION('center_axis',(0.,-1.,0.));
#5819=DIRECTION('ref_axis',(1.,0.,0.));
#5820=DIRECTION('center_axis',(0.,-1.,0.));
#5821=DIRECTION('ref_axis',(1.,0.,0.));
#5822=DIRECTION('center_axis',(0.,-1.,0.));
#5823=DIRECTION('ref_axis',(1.,0.,0.));
#5824=DIRECTION('',(0.707106781186547,0.707106781186548,8.65956056235493E-17));
#5825=DIRECTION('center_axis',(0.,-1.,0.));
#5826=DIRECTION('ref_axis',(1.,0.,0.));
#5827=DIRECTION('center_axis',(0.,1.,0.));
#5828=DIRECTION('ref_axis',(1.,0.,0.));
#5829=DIRECTION('',(0.,1.,0.));
#5830=DIRECTION('center_axis',(0.,1.,0.));
#5831=DIRECTION('ref_axis',(1.,0.,0.));
#5832=DIRECTION('center_axis',(0.,-1.,0.));
#5833=DIRECTION('ref_axis',(1.,0.,0.));
#5834=DIRECTION('',(-0.707106781186547,0.707106781186548,-8.65956056235493E-17));
#5835=DIRECTION('center_axis',(0.,-1.,0.));
#5836=DIRECTION('ref_axis',(0.,0.,-1.));
#7139=CARTESIAN_POINT('',(0.,0.,0.));
#7140=CARTESIAN_POINT('Origin',(0.0721687836487032,0.,-0.125));
#7141=CARTESIAN_POINT('',(0.0721687836487032,0.,-0.125));
#7142=CARTESIAN_POINT('',(0.144337567297406,0.,0.));
#7143=CARTESIAN_POINT('',(0.117710979560879,0.,-0.0461186027918559));
#7144=CARTESIAN_POINT('',(0.0721687836487032,-0.25,-0.125));
#7145=CARTESIAN_POINT('',(0.0721687836487032,0.,-0.125));
#7146=CARTESIAN_POINT('',(0.144337567297406,-0.25,0.));
#7147=CARTESIAN_POINT('',(0.144337567297406,-0.25,0.));
#7148=CARTESIAN_POINT('',(0.144337567297406,0.,0.));
#7149=CARTESIAN_POINT('Origin',(-0.0721687836487032,0.,-0.125));
#7150=CARTESIAN_POINT('',(-0.0721687836487032,0.,-0.125));
#7151=CARTESIAN_POINT('',(0.0739156081756484,0.,-0.125));
#7152=CARTESIAN_POINT('',(-0.0721687836487032,-0.25,-0.125));
#7153=CARTESIAN_POINT('',(-0.0721687836487032,0.,-0.125));
#7154=CARTESIAN_POINT('',(0.0721687836487032,-0.25,-0.125));
#7155=CARTESIAN_POINT('Origin',(-0.144337567297406,0.,-4.16333634234434E-17));
#7156=CARTESIAN_POINT('',(-0.144337567297406,0.,-1.76762539787485E-17));
#7157=CARTESIAN_POINT('',(-0.0987953713852306,0.,-0.0788813972081442));
#7158=CARTESIAN_POINT('',(-0.144337567297406,-0.25,-2.77555756156289E-17));
#7159=CARTESIAN_POINT('',(-0.144337567297406,0.,-1.76762539787485E-17));
#7160=CARTESIAN_POINT('',(-0.0721687836487032,-0.25,-0.125));
#7161=CARTESIAN_POINT('Origin',(-0.0721687836487033,0.,0.125));
#7162=CARTESIAN_POINT('',(-0.0721687836487033,0.,0.125));
#7163=CARTESIAN_POINT('',(-0.0627109795608791,0.,0.141381397208144));
#7164=CARTESIAN_POINT('',(-0.0721687836487033,-0.25,0.125));
#7165=CARTESIAN_POINT('',(-0.0721687836487033,0.,0.125));
#7166=CARTESIAN_POINT('',(-0.144337567297406,-0.25,-1.76762539787485E-17));
#7167=CARTESIAN_POINT('Origin',(0.0721687836487032,0.,0.125));
#7168=CARTESIAN_POINT('',(0.0721687836487032,0.,0.125));
#7169=CARTESIAN_POINT('',(0.146084391824352,0.,0.125));
#7170=CARTESIAN_POINT('',(0.0721687836487032,-0.25,0.125));
#7171=CARTESIAN_POINT('',(0.0721687836487032,0.,0.125));
#7172=CARTESIAN_POINT('',(-0.0721687836487033,-0.25,0.125));
#7173=CARTESIAN_POINT('Origin',(0.144337567297406,0.,0.));
#7174=CARTESIAN_POINT('',(0.153795371385231,0.,-0.0163813972081441));
#7175=CARTESIAN_POINT('',(0.0721687836487032,-0.25,0.125));
#7176=CARTESIAN_POINT('Origin',(0.,-0.25,0.));
#7177=CARTESIAN_POINT('Origin',(0.22,0.,0.));
#7178=CARTESIAN_POINT('',(-0.22,-8.67361737988404E-18,-2.69422295812418E-17));
#7179=CARTESIAN_POINT('Origin',(0.,0.,0.));
#7180=CARTESIAN_POINT('Origin',(0.,-0.015,0.));
#7181=CARTESIAN_POINT('',(-0.24505,-0.02505,-3.00099698131059E-17));
#7182=CARTESIAN_POINT('Origin',(0.,-0.02505,0.));
#7183=CARTESIAN_POINT('',(-0.235,-0.015,-2.87791997799628E-17));
#7184=CARTESIAN_POINT('Origin',(0.,-0.3775,0.));
#7185=CARTESIAN_POINT('',(-0.24505,-0.72995,3.00099698131059E-17));
#7186=CARTESIAN_POINT('Origin',(0.,-0.72995,0.));
#7187=CARTESIAN_POINT('',(-0.24505,-0.3775,-3.00099698131059E-17));
#7188=CARTESIAN_POINT('Origin',(0.,-0.7625,0.));
#7189=CARTESIAN_POINT('',(-0.175,-0.8,-2.14313189850787E-17));
#7190=CARTESIAN_POINT('Origin',(0.,-0.8,0.));
#7191=CARTESIAN_POINT('',(-0.2125,-0.7625,-2.60237444818813E-17));
#7192=CARTESIAN_POINT('Origin',(0.,-0.8,0.));
#7322=UNCERTAINTY_MEASURE_WITH_UNIT(LENGTH_MEASURE(0.001),#7350,
'DISTANCE_ACCURACY_VALUE',
'Maximum model space distance between geometric entities at asserted c
onnectivities');
#7324=UNCERTAINTY_MEASURE_WITH_UNIT(LENGTH_MEASURE(0.001),#7350,
'DISTANCE_ACCURACY_VALUE',
'Maximum model space distance between geometric entities at asserted c
onnectivities');
#7347=(
GEOMETRIC_REPRESENTATION_CONTEXT(3)
GLOBAL_UNCERTAINTY_ASSIGNED_CONTEXT((#7322))
GLOBAL_UNIT_ASSIGNED_CONTEXT((#7350,#7352,#7353))
REPRESENTATION_CONTEXT('','3D')
);
#7349=(
GEOMETRIC_REPRESENTATION_CONTEXT(3)
GLOBAL_UNCERTAINTY_ASSIGNED_CONTEXT((#7324))
GLOBAL_UNIT_ASSIGNED_CONTEXT((#7350,#7352,#7353))
REPRESENTATION_CONTEXT('','3D')
);
#7350=(
LENGTH_UNIT()
NAMED_UNIT(*)
SI_UNIT(.CENTI.,.METRE.)
);
#7352=(
NAMED_UNIT(*)
PLANE_ANGLE_UNIT()
SI_UNIT($,.RADIAN.)
);
#7353=(
NAMED_UNIT(*)
SI_UNIT($,.STERADIAN.)
SOLID_ANGLE_UNIT()
);
#7376=SHAPE_DEFINITION_REPRESENTATION(#7402,#7463);
#7402=PRODUCT_DEFINITION_SHAPE('',$,#7488);
#7463=SHAPE_REPRESENTATION('',(#4627),#7347);
#7465=PRODUCT_DEFINITION_CONTEXT('part definition',#7539,'design');
#7488=PRODUCT_DEFINITION('Socket Set Screw - M5x8',
'Socket Set Screw - M5x8',#7512,#7465);
#7512=PRODUCT_DEFINITION_FORMATION('',$,#7563);
#7539=APPLICATION_CONTEXT(
'Core Data for Automotive Mechanical Design Process');
#7540=PRODUCT_CONTEXT('part definition',#7539,'mechanical');
#7563=PRODUCT('Socket Set Screw - M5x8','Socket Set Screw - M5x8',
'Socket Set Screw - M5x8',(#7540));
#7628=COLOUR_RGB('Black',0.12,0.14,0.17);
#7629=FILL_AREA_STYLE_COLOUR('',#7628);
#7630=FILL_AREA_STYLE('',(#7629));
#7631=SURFACE_STYLE_FILL_AREA(#7630);
#7632=SURFACE_SIDE_STYLE('',(#7631));
#7633=SURFACE_STYLE_USAGE(.BOTH.,#7632);
#7634=PRESENTATION_STYLE_ASSIGNMENT((#7633));
ENDSEC;
END-ISO-10303-21;
